ISO-10303-21;
HEADER;
/* Generated by software containing ST-Developer
 * from STEP Tools, Inc. (www.steptools.com) 
 */

FILE_DESCRIPTION(
/* description */ ('', 'CAx-IF Rec.Pracs.---Representation and Presentation of Product Manufa
cturing Information (PMI)---4.0---2014-10-13'),
/* implementation_level */ '2;1');

FILE_NAME(
/* name */ 'Chamber Front Plate Socket Screws.step',
/* time_stamp */ '2026-10-28T23:00:48+01:00',
/* author */ (''),
/* organization */ (''),
/* preprocessor_version */ 'ST-DEVELOPER v20.2',
/* originating_system */ 'Autodesk Translation Framework v15.17.0.0',
/* authorisation */ '');

FILE_SCHEMA (('AP242_MANAGED_MODEL_BASED_3D_ENGINEERING_MIM_LF { 1 0 10303 442 2 1 4 }'));
ENDSEC;

DATA;
#10=MECHANICAL_DESIGN_GEOMETRIC_PRESENTATION_REPRESENTATION('',(#964),#61811);
#483=(
BOUNDED_CURVE()
B_SPLINE_CURVE(2,(#51098,#51099,#51100),.UNSPECIFIED.,.F.,.F.)
B_SPLINE_CURVE_WITH_KNOTS((3,3),(0.,0.467374455231167),.UNSPECIFIED.)
CURVE()
GEOMETRIC_REPRESENTATION_ITEM()
RATIONAL_B_SPLINE_CURVE((1.,1.15470053837925,1.))
REPRESENTATION_ITEM('')
);
#484=(
BOUNDED_CURVE()
B_SPLINE_CURVE(2,(#51105,#51106,#51107),.UNSPECIFIED.,.F.,.F.)
B_SPLINE_CURVE_WITH_KNOTS((3,3),(0.,0.467374455231167),.UNSPECIFIED.)
CURVE()
GEOMETRIC_REPRESENTATION_ITEM()
RATIONAL_B_SPLINE_CURVE((1.,1.15470053837925,1.))
REPRESENTATION_ITEM('')
);
#485=(
BOUNDED_CURVE()
B_SPLINE_CURVE(2,(#51111,#51112,#51113),.UNSPECIFIED.,.F.,.F.)
B_SPLINE_CURVE_WITH_KNOTS((3,3),(0.,0.467374455231166),.UNSPECIFIED.)
CURVE()
GEOMETRIC_REPRESENTATION_ITEM()
RATIONAL_B_SPLINE_CURVE((1.,1.15470053837925,1.))
REPRESENTATION_ITEM('')
);
#486=(
BOUNDED_CURVE()
B_SPLINE_CURVE(2,(#51117,#51118,#51119),.UNSPECIFIED.,.F.,.F.)
B_SPLINE_CURVE_WITH_KNOTS((3,3),(0.,0.467374455231167),.UNSPECIFIED.)
CURVE()
GEOMETRIC_REPRESENTATION_ITEM()
RATIONAL_B_SPLINE_CURVE((1.,1.15470053837926,1.))
REPRESENTATION_ITEM('')
);
#487=(
BOUNDED_CURVE()
B_SPLINE_CURVE(2,(#51123,#51124,#51125),.UNSPECIFIED.,.F.,.F.)
B_SPLINE_CURVE_WITH_KNOTS((3,3),(0.,0.233687227615585),.UNSPECIFIED.)
CURVE()
GEOMETRIC_REPRESENTATION_ITEM()
RATIONAL_B_SPLINE_CURVE((1.,1.07735026918963,1.07735026918963))
REPRESENTATION_ITEM('')
);
#488=(
BOUNDED_CURVE()
B_SPLINE_CURVE(2,(#51128,#51129,#51130),.UNSPECIFIED.,.F.,.F.)
B_SPLINE_CURVE_WITH_KNOTS((3,3),(0.233687227615585,0.467374455231167),
 .UNSPECIFIED.)
CURVE()
GEOMETRIC_REPRESENTATION_ITEM()
RATIONAL_B_SPLINE_CURVE((1.07735026918963,1.07735026918962,1.))
REPRESENTATION_ITEM('')
);
#489=(
BOUNDED_CURVE()
B_SPLINE_CURVE(2,(#51132,#51133,#51134),.UNSPECIFIED.,.F.,.F.)
B_SPLINE_CURVE_WITH_KNOTS((3,3),(0.,0.467374455231167),.UNSPECIFIED.)
CURVE()
GEOMETRIC_REPRESENTATION_ITEM()
RATIONAL_B_SPLINE_CURVE((1.,1.15470053837925,1.))
REPRESENTATION_ITEM('')
);
#567=CONICAL_SURFACE('',#34431,4.5399125,0.785398163397448);
#568=CONICAL_SURFACE('',#34447,2.3094010767585,1.0471975511966);
#890=TOROIDAL_SURFACE('',#34421,5.1,0.1);
#891=TOROIDAL_SURFACE('',#34434,7.,1.);
#914=SHAPE_REPRESENTATION_RELATIONSHIP('SRR','None',#61972,#939);
#939=ADVANCED_BREP_SHAPE_REPRESENTATION('',(#1003),#61785);
#964=STYLED_ITEM('',(#62163),#1003);
#1003=MANIFOLD_SOLID_BREP('Body1',#33794);
#1095=CYLINDRICAL_SURFACE('',#34426,5.);
#1096=CYLINDRICAL_SURFACE('',#34440,8.);
#1899=FACE_BOUND('',#6289,.T.);
#1900=FACE_BOUND('',#6294,.T.);
#2397=CIRCLE('',#34422,5.);
#2398=CIRCLE('',#34423,5.);
#2399=CIRCLE('',#34424,0.1);
#2400=CIRCLE('',#34425,5.1);
#2401=CIRCLE('',#34427,5.);
#2402=CIRCLE('',#34428,5.);
#2403=CIRCLE('',#34430,8.);
#2404=CIRCLE('',#34432,4.079825);
#2405=CIRCLE('',#34435,8.);
#2406=CIRCLE('',#34436,8.);
#2407=CIRCLE('',#34437,1.);
#2408=CIRCLE('',#34438,7.);
#4387=FACE_OUTER_BOUND('',#6286,.T.);
#4388=FACE_OUTER_BOUND('',#6287,.T.);
#4389=FACE_OUTER_BOUND('',#6288,.T.);
#4390=FACE_OUTER_BOUND('',#6290,.T.);
#4391=FACE_OUTER_BOUND('',#6291,.T.);
#4392=FACE_OUTER_BOUND('',#6292,.T.);
#4393=FACE_OUTER_BOUND('',#6293,.T.);
#4394=FACE_OUTER_BOUND('',#6295,.T.);
#4395=FACE_OUTER_BOUND('',#6296,.T.);
#4396=FACE_OUTER_BOUND('',#6297,.T.);
#4397=FACE_OUTER_BOUND('',#6298,.T.);
#4398=FACE_OUTER_BOUND('',#6299,.T.);
#4399=FACE_OUTER_BOUND('',#6300,.T.);
#4400=FACE_OUTER_BOUND('',#6301,.T.);
#4401=FACE_OUTER_BOUND('',#6302,.T.);
#6286=EDGE_LOOP('',(#22158,#22159,#22160,#22161,#22162));
#6287=EDGE_LOOP('',(#22163,#22164,#22165,#22166,#22167,#22168));
#6288=EDGE_LOOP('',(#22169));
#6289=EDGE_LOOP('',(#22170));
#6290=EDGE_LOOP('',(#22171,#22172,#22173,#22174,#22175));
#6291=EDGE_LOOP('',(#22176));
#6292=EDGE_LOOP('',(#22177,#22178,#22179,#22180,#22181));
#6293=EDGE_LOOP('',(#22182));
#6294=EDGE_LOOP('',(#22183,#22184,#22185,#22186,#22187,#22188));
#6295=EDGE_LOOP('',(#22189,#22190,#22191,#22192,#22193));
#6296=EDGE_LOOP('',(#22194,#22195,#22196,#22197));
#6297=EDGE_LOOP('',(#22198,#22199,#22200,#22201));
#6298=EDGE_LOOP('',(#22202,#22203,#22204,#22205));
#6299=EDGE_LOOP('',(#22206,#22207,#22208,#22209));
#6300=EDGE_LOOP('',(#22210,#22211,#22212,#22213,#22214));
#6301=EDGE_LOOP('',(#22215,#22216,#22217,#22218));
#6302=EDGE_LOOP('',(#22219,#22220,#22221,#22222,#22223,#22224,#22225,#22226,
#22227));
#8493=LINE('',#51063,#11040);
#8494=LINE('',#51069,#11041);
#8495=LINE('',#51083,#11042);
#8496=LINE('',#51085,#11043);
#8497=LINE('',#51087,#11044);
#8498=LINE('',#51089,#11045);
#8499=LINE('',#51091,#11046);
#8500=LINE('',#51092,#11047);
#8501=LINE('',#51094,#11048);
#8502=LINE('',#51101,#11049);
#8503=LINE('',#51102,#11050);
#8504=LINE('',#51108,#11051);
#8505=LINE('',#51114,#11052);
#8506=LINE('',#51120,#11053);
#8507=LINE('',#51127,#11054);
#8508=LINE('',#51137,#11055);
#11040=VECTOR('',#38947,5.);
#11041=VECTOR('',#38954,4.5399125);
#11042=VECTOR('',#38971,10.);
#11043=VECTOR('',#38972,10.);
#11044=VECTOR('',#38973,10.);
#11045=VECTOR('',#38974,10.);
#11046=VECTOR('',#38975,9.99999999999999);
#11047=VECTOR('',#38976,10.);
#11048=VECTOR('',#38979,8.);
#11049=VECTOR('',#38982,10.);
#11050=VECTOR('',#38983,10.);
#11051=VECTOR('',#38986,10.);
#11052=VECTOR('',#38989,10.);
#11053=VECTOR('',#38992,10.);
#11054=VECTOR('',#38995,10.);
#11055=VECTOR('',#39000,2.3094010767585);
#13650=VERTEX_POINT('',#51051);
#13651=VERTEX_POINT('',#51052);
#13652=VERTEX_POINT('',#51055);
#13653=VERTEX_POINT('',#51059);
#13654=VERTEX_POINT('',#51060);
#13655=VERTEX_POINT('',#51065);
#13656=VERTEX_POINT('',#51068);
#13657=VERTEX_POINT('',#51073);
#13658=VERTEX_POINT('',#51074);
#13659=VERTEX_POINT('',#51077);
#13660=VERTEX_POINT('',#51081);
#13661=VERTEX_POINT('',#51082);
#13662=VERTEX_POINT('',#51084);
#13663=VERTEX_POINT('',#51086);
#13664=VERTEX_POINT('',#51088);
#13665=VERTEX_POINT('',#51090);
#13666=VERTEX_POINT('',#51096);
#13667=VERTEX_POINT('',#51097);
#13668=VERTEX_POINT('',#51104);
#13669=VERTEX_POINT('',#51110);
#13670=VERTEX_POINT('',#51116);
#13671=VERTEX_POINT('',#51122);
#13672=VERTEX_POINT('',#51126);
#13673=VERTEX_POINT('',#51136);
#16981=EDGE_CURVE('',#13650,#13651,#2397,.T.);
#16982=EDGE_CURVE('',#13651,#13650,#2398,.T.);
#16983=EDGE_CURVE('',#13650,#13652,#2399,.T.);
#16984=EDGE_CURVE('',#13652,#13652,#2400,.T.);
#16985=EDGE_CURVE('',#13653,#13654,#2401,.T.);
#16986=EDGE_CURVE('',#13654,#13653,#2402,.T.);
#16987=EDGE_CURVE('',#13654,#13651,#8493,.T.);
#16988=EDGE_CURVE('',#13655,#13655,#2403,.T.);
#16989=EDGE_CURVE('',#13653,#13656,#8494,.T.);
#16990=EDGE_CURVE('',#13656,#13656,#2404,.T.);
#16991=EDGE_CURVE('',#13657,#13658,#2405,.T.);
#16992=EDGE_CURVE('',#13658,#13657,#2406,.T.);
#16993=EDGE_CURVE('',#13657,#13659,#2407,.T.);
#16994=EDGE_CURVE('',#13659,#13659,#2408,.T.);
#16995=EDGE_CURVE('',#13660,#13661,#8495,.T.);
#16996=EDGE_CURVE('',#13661,#13662,#8496,.T.);
#16997=EDGE_CURVE('',#13662,#13663,#8497,.T.);
#16998=EDGE_CURVE('',#13663,#13664,#8498,.T.);
#16999=EDGE_CURVE('',#13664,#13665,#8499,.T.);
#17000=EDGE_CURVE('',#13665,#13660,#8500,.T.);
#17001=EDGE_CURVE('',#13655,#13658,#8501,.T.);
#17002=EDGE_CURVE('',#13666,#13667,#483,.T.);
#17003=EDGE_CURVE('',#13666,#13665,#8502,.T.);
#17004=EDGE_CURVE('',#13667,#13664,#8503,.T.);
#17005=EDGE_CURVE('',#13668,#13666,#484,.T.);
#17006=EDGE_CURVE('',#13668,#13660,#8504,.T.);
#17007=EDGE_CURVE('',#13669,#13668,#485,.T.);
#17008=EDGE_CURVE('',#13669,#13661,#8505,.T.);
#17009=EDGE_CURVE('',#13670,#13669,#486,.T.);
#17010=EDGE_CURVE('',#13662,#13670,#8506,.T.);
#17011=EDGE_CURVE('',#13667,#13671,#487,.T.);
#17012=EDGE_CURVE('',#13672,#13663,#8507,.T.);
#17013=EDGE_CURVE('',#13671,#13672,#488,.T.);
#17014=EDGE_CURVE('',#13672,#13670,#489,.T.);
#17015=EDGE_CURVE('',#13673,#13671,#8508,.T.);
#22158=ORIENTED_EDGE('',*,*,#16981,.T.);
#22159=ORIENTED_EDGE('',*,*,#16982,.T.);
#22160=ORIENTED_EDGE('',*,*,#16983,.T.);
#22161=ORIENTED_EDGE('',*,*,#16984,.T.);
#22162=ORIENTED_EDGE('',*,*,#16983,.F.);
#22163=ORIENTED_EDGE('',*,*,#16985,.F.);
#22164=ORIENTED_EDGE('',*,*,#16986,.F.);
#22165=ORIENTED_EDGE('',*,*,#16987,.T.);
#22166=ORIENTED_EDGE('',*,*,#16981,.F.);
#22167=ORIENTED_EDGE('',*,*,#16982,.F.);
#22168=ORIENTED_EDGE('',*,*,#16987,.F.);
#22169=ORIENTED_EDGE('',*,*,#16988,.T.);
#22170=ORIENTED_EDGE('',*,*,#16984,.F.);
#22171=ORIENTED_EDGE('',*,*,#16985,.T.);
#22172=ORIENTED_EDGE('',*,*,#16986,.T.);
#22173=ORIENTED_EDGE('',*,*,#16989,.T.);
#22174=ORIENTED_EDGE('',*,*,#16990,.T.);
#22175=ORIENTED_EDGE('',*,*,#16989,.F.);
#22176=ORIENTED_EDGE('',*,*,#16990,.F.);
#22177=ORIENTED_EDGE('',*,*,#16991,.T.);
#22178=ORIENTED_EDGE('',*,*,#16992,.T.);
#22179=ORIENTED_EDGE('',*,*,#16993,.T.);
#22180=ORIENTED_EDGE('',*,*,#16994,.T.);
#22181=ORIENTED_EDGE('',*,*,#16993,.F.);
#22182=ORIENTED_EDGE('',*,*,#16994,.F.);
#22183=ORIENTED_EDGE('',*,*,#16995,.T.);
#22184=ORIENTED_EDGE('',*,*,#16996,.T.);
#22185=ORIENTED_EDGE('',*,*,#16997,.T.);
#22186=ORIENTED_EDGE('',*,*,#16998,.T.);
#22187=ORIENTED_EDGE('',*,*,#16999,.T.);
#22188=ORIENTED_EDGE('',*,*,#17000,.T.);
#22189=ORIENTED_EDGE('',*,*,#16988,.F.);
#22190=ORIENTED_EDGE('',*,*,#17001,.T.);
#22191=ORIENTED_EDGE('',*,*,#16991,.F.);
#22192=ORIENTED_EDGE('',*,*,#16992,.F.);
#22193=ORIENTED_EDGE('',*,*,#17001,.F.);
#22194=ORIENTED_EDGE('',*,*,#17002,.F.);
#22195=ORIENTED_EDGE('',*,*,#17003,.T.);
#22196=ORIENTED_EDGE('',*,*,#16999,.F.);
#22197=ORIENTED_EDGE('',*,*,#17004,.F.);
#22198=ORIENTED_EDGE('',*,*,#17005,.F.);
#22199=ORIENTED_EDGE('',*,*,#17006,.T.);
#22200=ORIENTED_EDGE('',*,*,#17000,.F.);
#22201=ORIENTED_EDGE('',*,*,#17003,.F.);
#22202=ORIENTED_EDGE('',*,*,#17007,.F.);
#22203=ORIENTED_EDGE('',*,*,#17008,.T.);
#22204=ORIENTED_EDGE('',*,*,#16995,.F.);
#22205=ORIENTED_EDGE('',*,*,#17006,.F.);
#22206=ORIENTED_EDGE('',*,*,#17009,.F.);
#22207=ORIENTED_EDGE('',*,*,#17010,.F.);
#22208=ORIENTED_EDGE('',*,*,#16996,.F.);
#22209=ORIENTED_EDGE('',*,*,#17008,.F.);
#22210=ORIENTED_EDGE('',*,*,#17011,.F.);
#22211=ORIENTED_EDGE('',*,*,#17004,.T.);
#22212=ORIENTED_EDGE('',*,*,#16998,.F.);
#22213=ORIENTED_EDGE('',*,*,#17012,.F.);
#22214=ORIENTED_EDGE('',*,*,#17013,.F.);
#22215=ORIENTED_EDGE('',*,*,#17014,.F.);
#22216=ORIENTED_EDGE('',*,*,#17012,.T.);
#22217=ORIENTED_EDGE('',*,*,#16997,.F.);
#22218=ORIENTED_EDGE('',*,*,#17010,.T.);
#22219=ORIENTED_EDGE('',*,*,#17015,.T.);
#22220=ORIENTED_EDGE('',*,*,#17013,.T.);
#22221=ORIENTED_EDGE('',*,*,#17014,.T.);
#22222=ORIENTED_EDGE('',*,*,#17009,.T.);
#22223=ORIENTED_EDGE('',*,*,#17007,.T.);
#22224=ORIENTED_EDGE('',*,*,#17005,.T.);
#22225=ORIENTED_EDGE('',*,*,#17002,.T.);
#22226=ORIENTED_EDGE('',*,*,#17011,.T.);
#22227=ORIENTED_EDGE('',*,*,#17015,.F.);
#31160=PLANE('',#34429);
#31161=PLANE('',#34433);
#31162=PLANE('',#34439);
#31163=PLANE('',#34441);
#31164=PLANE('',#34442);
#31165=PLANE('',#34443);
#31166=PLANE('',#34444);
#31167=PLANE('',#34445);
#31168=PLANE('',#34446);
#32068=ADVANCED_FACE('',(#4387),#890,.F.);
#32069=ADVANCED_FACE('',(#4388),#1095,.T.);
#32070=ADVANCED_FACE('',(#4389,#1899),#31160,.T.);
#32071=ADVANCED_FACE('',(#4390),#567,.T.);
#32072=ADVANCED_FACE('',(#4391),#31161,.T.);
#32073=ADVANCED_FACE('',(#4392),#891,.T.);
#32074=ADVANCED_FACE('',(#4393,#1900),#31162,.T.);
#32075=ADVANCED_FACE('',(#4394),#1096,.T.);
#32076=ADVANCED_FACE('',(#4395),#31163,.F.);
#32077=ADVANCED_FACE('',(#4396),#31164,.F.);
#32078=ADVANCED_FACE('',(#4397),#31165,.F.);
#32079=ADVANCED_FACE('',(#4398),#31166,.F.);
#32080=ADVANCED_FACE('',(#4399),#31167,.F.);
#32081=ADVANCED_FACE('',(#4400),#31168,.F.);
#32082=ADVANCED_FACE('',(#4401),#568,.F.);
#33794=CLOSED_SHELL('',(#32068,#32069,#32070,#32071,#32072,#32073,#32074,
#32075,#32076,#32077,#32078,#32079,#32080,#32081,#32082));
#34420=AXIS2_PLACEMENT_3D('',#51049,#38929,#38930);
#34421=AXIS2_PLACEMENT_3D('',#51050,#38931,#38932);
#34422=AXIS2_PLACEMENT_3D('',#51053,#38933,#38934);
#34423=AXIS2_PLACEMENT_3D('',#51054,#38935,#38936);
#34424=AXIS2_PLACEMENT_3D('',#51056,#38937,#38938);
#34425=AXIS2_PLACEMENT_3D('',#51057,#38939,#38940);
#34426=AXIS2_PLACEMENT_3D('',#51058,#38941,#38942);
#34427=AXIS2_PLACEMENT_3D('',#51061,#38943,#38944);
#34428=AXIS2_PLACEMENT_3D('',#51062,#38945,#38946);
#34429=AXIS2_PLACEMENT_3D('',#51064,#38948,#38949);
#34430=AXIS2_PLACEMENT_3D('',#51066,#38950,#38951);
#34431=AXIS2_PLACEMENT_3D('',#51067,#38952,#38953);
#34432=AXIS2_PLACEMENT_3D('',#51070,#38955,#38956);
#34433=AXIS2_PLACEMENT_3D('',#51071,#38957,#38958);
#34434=AXIS2_PLACEMENT_3D('',#51072,#38959,#38960);
#34435=AXIS2_PLACEMENT_3D('',#51075,#38961,#38962);
#34436=AXIS2_PLACEMENT_3D('',#51076,#38963,#38964);
#34437=AXIS2_PLACEMENT_3D('',#51078,#38965,#38966);
#34438=AXIS2_PLACEMENT_3D('',#51079,#38967,#38968);
#34439=AXIS2_PLACEMENT_3D('',#51080,#38969,#38970);
#34440=AXIS2_PLACEMENT_3D('',#51093,#38977,#38978);
#34441=AXIS2_PLACEMENT_3D('',#51095,#38980,#38981);
#34442=AXIS2_PLACEMENT_3D('',#51103,#38984,#38985);
#34443=AXIS2_PLACEMENT_3D('',#51109,#38987,#38988);
#34444=AXIS2_PLACEMENT_3D('',#51115,#38990,#38991);
#34445=AXIS2_PLACEMENT_3D('',#51121,#38993,#38994);
#34446=AXIS2_PLACEMENT_3D('',#51131,#38996,#38997);
#34447=AXIS2_PLACEMENT_3D('',#51135,#38998,#38999);
#38929=DIRECTION('axis',(0.,0.,1.));
#38930=DIRECTION('refdir',(1.,0.,0.));
#38931=DIRECTION('center_axis',(-1.,5.00264601743691E-16,3.82282413363175E-15));
#38932=DIRECTION('ref_axis',(0.,0.,1.));
#38933=DIRECTION('center_axis',(1.,-5.00264601743691E-16,-3.82282413363175E-15));
#38934=DIRECTION('ref_axis',(-5.00264601743696E-16,-1.,-1.24274386213125E-15));
#38935=DIRECTION('center_axis',(1.,-5.00264601743691E-16,-3.82282413363175E-15));
#38936=DIRECTION('ref_axis',(-5.00264601743696E-16,-1.,-1.24274386213125E-15));
#38937=DIRECTION('center_axis',(5.00264601743691E-16,1.,0.));
#38938=DIRECTION('ref_axis',(0.,0.,-1.));
#38939=DIRECTION('center_axis',(-1.,5.00264601743691E-16,3.82282413363175E-15));
#38940=DIRECTION('ref_axis',(-5.00264601743696E-16,-1.,-1.24274386213126E-15));
#38941=DIRECTION('center_axis',(-1.,5.00264601743691E-16,3.82282413363175E-15));
#38942=DIRECTION('ref_axis',(5.00264601743695E-16,1.,1.12027918221652E-15));
#38943=DIRECTION('center_axis',(-1.,5.00264601743691E-16,3.82282413363175E-15));
#38944=DIRECTION('ref_axis',(-5.00264601743695E-16,-1.,-1.12027918221652E-15));
#38945=DIRECTION('center_axis',(-1.,5.00264601743691E-16,3.82282413363175E-15));
#38946=DIRECTION('ref_axis',(-5.00264601743695E-16,-1.,-1.12027918221652E-15));
#38947=DIRECTION('',(1.,-5.00264601743691E-16,-3.82282413363175E-15));
#38948=DIRECTION('center_axis',(-1.,5.00264601743691E-16,3.82282413363175E-15));
#38949=DIRECTION('ref_axis',(3.82282413363175E-15,-1.12027918221652E-15,
1.));
#38950=DIRECTION('center_axis',(-1.,5.00264601743691E-16,3.82282413363175E-15));
#38951=DIRECTION('ref_axis',(5.00264601743695E-16,1.,1.12027918221652E-15));
#38952=DIRECTION('center_axis',(1.,-5.00264601743691E-16,-3.82282413363175E-15));
#38953=DIRECTION('ref_axis',(-5.00264601743695E-16,-1.,-1.12027918221652E-15));
#38954=DIRECTION('',(-0.707106781186548,-0.707106781186547,1.82439225598363E-15));
#38955=DIRECTION('center_axis',(1.,-5.00264601743691E-16,-3.82282413363175E-15));
#38956=DIRECTION('ref_axis',(-5.00264601743695E-16,-1.,-1.12027918221652E-15));
#38957=DIRECTION('center_axis',(-1.,5.00264601743691E-16,3.82282413363175E-15));
#38958=DIRECTION('ref_axis',(3.82282413363175E-15,-1.12027918221652E-15,
1.));
#38959=DIRECTION('center_axis',(-1.,5.00264601743691E-16,3.82282413363175E-15));
#38960=DIRECTION('ref_axis',(0.,-1.77635683940025E-15,1.));
#38961=DIRECTION('center_axis',(1.,-5.00264601743691E-16,-3.82282413363175E-15));
#38962=DIRECTION('ref_axis',(-5.00264601743696E-16,-1.,-1.24274386213126E-15));
#38963=DIRECTION('center_axis',(1.,-5.00264601743691E-16,-3.82282413363175E-15));
#38964=DIRECTION('ref_axis',(-5.00264601743696E-16,-1.,-1.24274386213126E-15));
#38965=DIRECTION('center_axis',(-5.00264601743691E-16,-1.,0.));
#38966=DIRECTION('ref_axis',(0.,0.,-1.));
#38967=DIRECTION('center_axis',(-1.,5.00264601743691E-16,3.82282413363175E-15));
#38968=DIRECTION('ref_axis',(-5.00264601743696E-16,-1.,-1.24274386213125E-15));
#38969=DIRECTION('center_axis',(1.,-5.00264601743691E-16,-3.82282413363175E-15));
#38970=DIRECTION('ref_axis',(-3.82282413363175E-15,1.12027918221652E-15,
-1.));
#38971=DIRECTION('',(-3.82282413363175E-15,1.60101985381241E-15,-1.));
#38972=DIRECTION('',(-2.34465392054002E-15,-0.866025403784438,-0.500000000000001));
#38973=DIRECTION('',(1.47817021309173E-15,-0.866025403784439,0.499999999999999));
#38974=DIRECTION('',(3.82282413363175E-15,-1.2404643501155E-15,1.));
#38975=DIRECTION('',(2.34465392054002E-15,0.866025403784438,0.500000000000001));
#38976=DIRECTION('',(-1.47817021309173E-15,0.866025403784439,-0.499999999999999));
#38977=DIRECTION('center_axis',(-1.,5.00264601743691E-16,3.82282413363175E-15));
#38978=DIRECTION('ref_axis',(5.00264601743695E-16,1.,1.12027918221652E-15));
#38979=DIRECTION('',(1.,-5.00264601743691E-16,-3.82282413363175E-15));
#38980=DIRECTION('center_axis',(3.06053051305348E-15,-0.500000000000001,
0.866025403784438));
#38981=DIRECTION('ref_axis',(1.,-5.00513183386765E-16,-3.82296765231029E-15));
#38982=DIRECTION('',(1.,-5.00264601743691E-16,-3.82282413363175E-15));
#38983=DIRECTION('',(1.,-5.00264601743691E-16,-3.82282413363175E-15));
#38984=DIRECTION('center_axis',(3.56079511479718E-15,0.499999999999999,
0.866025403784439));
#38985=DIRECTION('ref_axis',(1.,-5.00513183386765E-16,-3.8226806149532E-15));
#38986=DIRECTION('',(1.,-5.00264601743691E-16,-3.82282413363175E-15));
#38987=DIRECTION('center_axis',(5.00264601743697E-16,1.,1.60101985381241E-15));
#38988=DIRECTION('ref_axis',(-3.82282413363175E-15,1.60101985381241E-15,
-1.));
#38989=DIRECTION('',(1.,-5.00264601743691E-16,-3.82282413363175E-15));
#38990=DIRECTION('center_axis',(-3.06053051305348E-15,0.500000000000001,
-0.866025403784438));
#38991=DIRECTION('ref_axis',(-1.,5.00513183386765E-16,3.82296765231029E-15));
#38992=DIRECTION('',(-1.,5.00264601743691E-16,3.82282413363175E-15));
#38993=DIRECTION('center_axis',(-5.00264601743696E-16,-1.,-1.24046435011549E-15));
#38994=DIRECTION('ref_axis',(3.82282413363175E-15,-1.2404643501155E-15,
1.));
#38995=DIRECTION('',(1.,-5.00264601743691E-16,-3.82282413363175E-15));
#38996=DIRECTION('center_axis',(-3.56079511479718E-15,-0.499999999999999,
-0.866025403784439));
#38997=DIRECTION('ref_axis',(-1.,5.00513183386765E-16,3.8226806149532E-15));
#38998=DIRECTION('center_axis',(1.,-5.00264601743691E-16,-3.82282413363175E-15));
#38999=DIRECTION('ref_axis',(5.00264601743695E-16,1.,1.12027918221652E-15));
#39000=DIRECTION('',(0.5,-0.866025403784439,-2.98765982181873E-15));
#51049=CARTESIAN_POINT('',(0.,0.,0.));
#51050=CARTESIAN_POINT('Origin',(474.015917770968,-92.9720072687899,380.000000551893));
#51051=CARTESIAN_POINT('',(474.015917770968,-92.9720072687899,375.000000551893));
#51052=CARTESIAN_POINT('',(474.015917770968,-97.9720072687899,380.000000551893));
#51053=CARTESIAN_POINT('Origin',(474.015917770968,-92.9720072687899,380.000000551893));
#51054=CARTESIAN_POINT('Origin',(474.015917770968,-92.9720072687899,380.000000551893));
#51055=CARTESIAN_POINT('',(474.115917770968,-92.9720072687899,374.900000551893));
#51056=CARTESIAN_POINT('Origin',(474.015917770968,-92.9720072687899,374.900000551893));
#51057=CARTESIAN_POINT('Origin',(474.115917770968,-92.9720072687899,380.000000551893));
#51058=CARTESIAN_POINT('Origin',(459.740917770968,-92.9720072687899,380.000000551893));
#51059=CARTESIAN_POINT('',(450.036092770968,-87.9720072687899,380.000000551893));
#51060=CARTESIAN_POINT('',(450.036092770968,-97.9720072687899,380.000000551893));
#51061=CARTESIAN_POINT('Origin',(450.036092770968,-92.9720072687899,380.000000551893));
#51062=CARTESIAN_POINT('Origin',(450.036092770968,-92.9720072687899,380.000000551893));
#51063=CARTESIAN_POINT('',(459.740917770968,-97.9720072687899,380.000000551893));
#51064=CARTESIAN_POINT('Origin',(474.115917770968,-86.4720072687899,380.000000551893));
#51065=CARTESIAN_POINT('',(474.115917770968,-100.97200726879,380.000000551893));
#51066=CARTESIAN_POINT('Origin',(474.115917770968,-92.9720072687899,380.000000551893));
#51067=CARTESIAN_POINT('Origin',(449.576005270968,-92.9720072687899,380.000000551893));
#51068=CARTESIAN_POINT('',(449.115917770968,-88.8921822687899,380.000000551893));
#51069=CARTESIAN_POINT('',(449.576005270968,-88.4320947687899,380.000000551893));
#51070=CARTESIAN_POINT('Origin',(449.115917770968,-92.9720072687899,380.000000551893));
#51071=CARTESIAN_POINT('Origin',(449.115917770968,-90.4720072687899,380.000000551893));
#51072=CARTESIAN_POINT('Origin',(483.115917770968,-92.9720072687899,380.000000551893));
#51073=CARTESIAN_POINT('',(483.115917770968,-92.9720072687899,372.000000551893));
#51074=CARTESIAN_POINT('',(483.115917770968,-100.97200726879,380.000000551893));
#51075=CARTESIAN_POINT('Origin',(483.115917770968,-92.9720072687899,380.000000551893));
#51076=CARTESIAN_POINT('Origin',(483.115917770968,-92.9720072687899,380.000000551893));
#51077=CARTESIAN_POINT('',(484.115917770968,-92.9720072687899,373.000000551893));
#51078=CARTESIAN_POINT('Origin',(483.115917770968,-92.9720072687899,373.000000551893));
#51079=CARTESIAN_POINT('Origin',(484.115917770968,-92.9720072687899,380.000000551893));
#51080=CARTESIAN_POINT('Origin',(484.115917770968,-86.6626061920314,380.000000551893));
#51081=CARTESIAN_POINT('',(484.115917770968,-88.9720072687899,382.309401628651));
#51082=CARTESIAN_POINT('',(484.115917770968,-88.9720072687899,377.690599475134));
#51083=CARTESIAN_POINT('',(484.115917770968,-88.9720072687899,378.845300013513));
#51084=CARTESIAN_POINT('',(484.115917770968,-92.9720072687899,375.381198398376));
#51085=CARTESIAN_POINT('',(484.115917770968,-91.9720072687899,375.958548667565));
#51086=CARTESIAN_POINT('',(484.115917770968,-96.9720072687899,377.690599475134));
#51087=CARTESIAN_POINT('',(484.115917770968,-95.9720072687899,377.113249205944));
#51088=CARTESIAN_POINT('',(484.115917770968,-96.9720072687899,382.309401628651));
#51089=CARTESIAN_POINT('',(484.115917770968,-96.9720072687899,381.154701090272));
#51090=CARTESIAN_POINT('',(484.115917770968,-92.97200726879,384.61880270541));
#51091=CARTESIAN_POINT('',(484.115917770968,-93.9720072687899,384.04145243622));
#51092=CARTESIAN_POINT('',(484.115917770968,-89.9720072687899,382.886751897841));
#51093=CARTESIAN_POINT('Origin',(479.115917770968,-92.9720072687899,380.000000551893));
#51094=CARTESIAN_POINT('',(479.115917770968,-100.97200726879,380.000000551893));
#51095=CARTESIAN_POINT('Origin',(484.115917770968,-92.97200726879,384.61880270541));
#51096=CARTESIAN_POINT('',(479.115917770968,-92.97200726879,384.61880270541));
#51097=CARTESIAN_POINT('',(479.115917770968,-96.9720072687899,382.309401628651));
#51098=CARTESIAN_POINT('Ctrl Pts',(479.115917770968,-92.97200726879,384.61880270541));
#51099=CARTESIAN_POINT('Ctrl Pts',(478.449251104301,-94.9720072687899,383.46410216703));
#51100=CARTESIAN_POINT('Ctrl Pts',(479.115917770968,-96.9720072687899,382.309401628651));
#51101=CARTESIAN_POINT('',(481.615917770968,-92.97200726879,384.61880270541));
#51102=CARTESIAN_POINT('',(481.615917770968,-96.9720072687899,382.309401628651));
#51103=CARTESIAN_POINT('Origin',(484.115917770968,-88.9720072687899,382.309401628651));
#51104=CARTESIAN_POINT('',(479.115917770968,-88.9720072687899,382.309401628651));
#51105=CARTESIAN_POINT('Ctrl Pts',(479.115917770968,-88.9720072687899,382.309401628651));
#51106=CARTESIAN_POINT('Ctrl Pts',(478.449251104301,-90.9720072687899,383.46410216703));
#51107=CARTESIAN_POINT('Ctrl Pts',(479.115917770968,-92.9720072687899,384.61880270541));
#51108=CARTESIAN_POINT('',(481.615917770968,-88.9720072687899,382.309401628651));
#51109=CARTESIAN_POINT('Origin',(484.115917770968,-88.9720072687899,377.690599475134));
#51110=CARTESIAN_POINT('',(479.115917770968,-88.9720072687899,377.690599475134));
#51111=CARTESIAN_POINT('Ctrl Pts',(479.115917770968,-88.9720072687899,377.690599475134));
#51112=CARTESIAN_POINT('Ctrl Pts',(478.449251104301,-88.9720072687899,380.000000551893));
#51113=CARTESIAN_POINT('Ctrl Pts',(479.115917770968,-88.9720072687899,382.309401628651));
#51114=CARTESIAN_POINT('',(481.615917770968,-88.9720072687899,377.690599475134));
#51115=CARTESIAN_POINT('Origin',(484.115917770968,-92.9720072687899,375.381198398376));
#51116=CARTESIAN_POINT('',(479.115917770968,-92.9720072687899,375.381198398376));
#51117=CARTESIAN_POINT('Ctrl Pts',(479.115917770968,-92.9720072687899,375.381198398376));
#51118=CARTESIAN_POINT('Ctrl Pts',(478.449251104301,-90.9720072687899,376.535898936755));
#51119=CARTESIAN_POINT('Ctrl Pts',(479.115917770968,-88.9720072687899,377.690599475134));
#51120=CARTESIAN_POINT('',(481.615917770968,-92.9720072687899,375.381198398376));
#51121=CARTESIAN_POINT('Origin',(484.115917770968,-96.9720072687899,382.309401628651));
#51122=CARTESIAN_POINT('',(478.75865218106,-96.9720072687899,380.000000551893));
#51123=CARTESIAN_POINT('Ctrl Pts',(479.115917770968,-96.9720072687899,382.309401628651));
#51124=CARTESIAN_POINT('Ctrl Pts',(478.75865218106,-96.9720072687899,381.071797321617));
#51125=CARTESIAN_POINT('Ctrl Pts',(478.75865218106,-96.9720072687899,380.000000551893));
#51126=CARTESIAN_POINT('',(479.115917770968,-96.9720072687899,377.690599475134));
#51127=CARTESIAN_POINT('',(481.615917770968,-96.9720072687899,377.690599475134));
#51128=CARTESIAN_POINT('Ctrl Pts',(478.75865218106,-96.9720072687899,380.000000551893));
#51129=CARTESIAN_POINT('Ctrl Pts',(478.75865218106,-96.9720072687899,378.928203782168));
#51130=CARTESIAN_POINT('Ctrl Pts',(479.115917770968,-96.9720072687899,377.690599475134));
#51131=CARTESIAN_POINT('Origin',(484.115917770968,-96.9720072687899,377.690599475134));
#51132=CARTESIAN_POINT('Ctrl Pts',(479.115917770968,-96.9720072687899,377.690599475134));
#51133=CARTESIAN_POINT('Ctrl Pts',(478.449251104301,-94.9720072687899,376.535898936755));
#51134=CARTESIAN_POINT('Ctrl Pts',(479.115917770968,-92.9720072687899,375.381198398376));
#51135=CARTESIAN_POINT('Origin',(477.782584437634,-92.9720072687899,380.000000551893));
#51136=CARTESIAN_POINT('',(476.449251104301,-92.9720072687899,380.000000551893));
#51137=CARTESIAN_POINT('',(477.782584437634,-95.2814083455484,380.000000551893));
#61754=UNCERTAINTY_MEASURE_WITH_UNIT(LENGTH_MEASURE(0.01),#61812,
'DISTANCE_ACCURACY_VALUE',
'Maximum model space distance between geometric entities at asserted c
onnectivities');
#61780=UNCERTAINTY_MEASURE_WITH_UNIT(LENGTH_MEASURE(0.01),#61812,
'DISTANCE_ACCURACY_VALUE',
'Maximum model space distance between geometric entities at asserted c
onnectivities');
#61785=(
GEOMETRIC_REPRESENTATION_CONTEXT(3)
GLOBAL_UNCERTAINTY_ASSIGNED_CONTEXT((#61754))
GLOBAL_UNIT_ASSIGNED_CONTEXT((#61812,#61814,#61815))
REPRESENTATION_CONTEXT('','3D')
);
#61811=(
GEOMETRIC_REPRESENTATION_CONTEXT(3)
GLOBAL_UNCERTAINTY_ASSIGNED_CONTEXT((#61780))
GLOBAL_UNIT_ASSIGNED_CONTEXT((#61812,#61814,#61815))
REPRESENTATION_CONTEXT('','3D')
);
#61812=(
LENGTH_UNIT()
NAMED_UNIT(*)
SI_UNIT(.MILLI.,.METRE.)
);
#61814=(
NAMED_UNIT(*)
PLANE_ANGLE_UNIT()
SI_UNIT($,.RADIAN.)
);
#61815=(
NAMED_UNIT(*)
SI_UNIT($,.STERADIAN.)
SOLID_ANGLE_UNIT()
);
#61820=SHAPE_DEFINITION_REPRESENTATION(#61850,#61972);
#61850=PRODUCT_DEFINITION_SHAPE('',$,#62003);
#61972=SHAPE_REPRESENTATION('',(#34420),#61785);
#61998=PRODUCT_DEFINITION_CONTEXT('part definition',#62090,'design');
#62003=PRODUCT_DEFINITION('Chamber Front Plate Socket Screws',
'Chamber Front Plate Socket Screws',#62033,#61998);
#62033=PRODUCT_DEFINITION_FORMATION('',$,#62096);
#62090=APPLICATION_CONTEXT('Managed model based 3d engineering');
#62091=PRODUCT_CONTEXT('part definition',#62090,'mechanical');
#62096=PRODUCT('Chamber Front Plate Socket Screws',
'Chamber Front Plate Socket Screws',$,(#62091));
#62157=COLOUR_RGB('Black',0.12,0.14,0.17);
#62158=FILL_AREA_STYLE_COLOUR('',#62157);
#62159=FILL_AREA_STYLE('',(#62158));
#62160=SURFACE_STYLE_FILL_AREA(#62159);
#62161=SURFACE_SIDE_STYLE('',(#62160));
#62162=SURFACE_STYLE_USAGE(.BOTH.,#62161);
#62163=PRESENTATION_STYLE_ASSIGNMENT((#62162));
ENDSEC;
END-ISO-10303-21;
